ISO-10303-21;
HEADER;
/* Generated by software containing ST-Developer
 * from STEP Tools, Inc. (www.steptools.com) 
 */

FILE_DESCRIPTION(
/* description */ ('Belt conveyor head drive unit'),
/* implementation_level */ '2;1');

FILE_NAME(
/* name */ 'Input M3 set screw.step',
/* time_stamp */ '2026-10-28T03:26:19-07:00',
/* author */ (''),
/* organization */ (''),
/* preprocessor_version */ 'ST-DEVELOPER v20.2',
/* originating_system */ 'Autodesk Translation Framework v15.17.0.0',
/* authorisation */ '');

FILE_SCHEMA (('AUTOMOTIVE_DESIGN { 1 0 10303 214 3 1 1 }'));
ENDSEC;

DATA;
#10=MECHANICAL_DESIGN_GEOMETRIC_PRESENTATION_REPRESENTATION('',(#910),#27069);
#756=SHAPE_REPRESENTATION_RELATIONSHIP('SRR','None',#27404,#825);
#825=ADVANCED_BREP_SHAPE_REPRESENTATION('',(#991),#27046);
#910=STYLED_ITEM('',(#27804),#991);
#991=MANIFOLD_SOLID_BREP('Body1',#13779);
#1552=PLANE('',#15685);
#1553=PLANE('',#15686);
#2168=FACE_OUTER_BOUND('',#3170,.T.);
#2169=FACE_OUTER_BOUND('',#3171,.T.);
#2170=FACE_OUTER_BOUND('',#3172,.T.);
#3170=EDGE_LOOP('',(#11220,#11221,#11222,#11223));
#3171=EDGE_LOOP('',(#11224));
#3172=EDGE_LOOP('',(#11225));
#4054=LINE('',#24520,#4846);
#4846=VECTOR('',#19234,0.15);
#5601=CIRCLE('',#15683,0.15);
#5602=CIRCLE('',#15684,0.15);
#6727=VERTEX_POINT('',#24517);
#6728=VERTEX_POINT('',#24519);
#8302=EDGE_CURVE('',#6727,#6727,#5601,.T.);
#8303=EDGE_CURVE('',#6727,#6728,#4054,.T.);
#8304=EDGE_CURVE('',#6728,#6728,#5602,.T.);
#11220=ORIENTED_EDGE('',*,*,#8302,.F.);
#11221=ORIENTED_EDGE('',*,*,#8303,.T.);
#11222=ORIENTED_EDGE('',*,*,#8304,.T.);
#11223=ORIENTED_EDGE('',*,*,#8303,.F.);
#11224=ORIENTED_EDGE('',*,*,#8302,.T.);
#11225=ORIENTED_EDGE('',*,*,#8304,.F.);
#12734=CYLINDRICAL_SURFACE('',#15682,0.15);
#13447=ADVANCED_FACE('',(#2168),#12734,.T.);
#13448=ADVANCED_FACE('',(#2169),#1552,.T.);
#13449=ADVANCED_FACE('',(#2170),#1553,.F.);
#13779=CLOSED_SHELL('',(#13447,#13448,#13449));
#15681=AXIS2_PLACEMENT_3D('',#24515,#19228,#19229);
#15682=AXIS2_PLACEMENT_3D('',#24516,#19230,#19231);
#15683=AXIS2_PLACEMENT_3D('',#24518,#19232,#19233);
#15684=AXIS2_PLACEMENT_3D('',#24521,#19235,#19236);
#15685=AXIS2_PLACEMENT_3D('',#24522,#19237,#19238);
#15686=AXIS2_PLACEMENT_3D('',#24523,#19239,#19240);
#19228=DIRECTION('axis',(0.,0.,1.));
#19229=DIRECTION('refdir',(1.,0.,0.));
#19230=DIRECTION('center_axis',(0.,0.,1.));
#19231=DIRECTION('ref_axis',(1.,0.,0.));
#19232=DIRECTION('center_axis',(0.,0.,1.));
#19233=DIRECTION('ref_axis',(1.,0.,0.));
#19234=DIRECTION('',(0.,0.,-1.));
#19235=DIRECTION('center_axis',(0.,0.,1.));
#19236=DIRECTION('ref_axis',(1.,0.,0.));
#19237=DIRECTION('center_axis',(0.,0.,1.));
#19238=DIRECTION('ref_axis',(1.,0.,0.));
#19239=DIRECTION('center_axis',(0.,0.,1.));
#19240=DIRECTION('ref_axis',(1.,0.,0.));
#24515=CARTESIAN_POINT('',(0.,0.,0.));
#24516=CARTESIAN_POINT('Origin',(0.,-3.95,6.35));
#24517=CARTESIAN_POINT('',(-0.15,-3.95,6.6));
#24518=CARTESIAN_POINT('Origin',(0.,-3.95,6.6));
#24519=CARTESIAN_POINT('',(-0.15,-3.95,6.35));
#24520=CARTESIAN_POINT('',(-0.15,-3.95,6.35));
#24521=CARTESIAN_POINT('Origin',(0.,-3.95,6.35));
#24522=CARTESIAN_POINT('Origin',(0.,-3.95,6.6));
#24523=CARTESIAN_POINT('Origin',(0.,-3.95,6.35));
#26969=UNCERTAINTY_MEASURE_WITH_UNIT(LENGTH_MEASURE(0.001),#27070,
'DISTANCE_ACCURACY_VALUE',
'Maximum model space distance between geometric entities at asserted c
onnectivities');
#26992=UNCERTAINTY_MEASURE_WITH_UNIT(LENGTH_MEASURE(0.001),#27070,
'DISTANCE_ACCURACY_VALUE',
'Maximum model space distance between geometric entities at asserted c
onnectivities');
#27046=(
GEOMETRIC_REPRESENTATION_CONTEXT(3)
GLOBAL_UNCERTAINTY_ASSIGNED_CONTEXT((#26969))
GLOBAL_UNIT_ASSIGNED_CONTEXT((#27070,#27072,#27073))
REPRESENTATION_CONTEXT('','3D')
);
#27069=(
GEOMETRIC_REPRESENTATION_CONTEXT(3)
GLOBAL_UNCERTAINTY_ASSIGNED_CONTEXT((#26992))
GLOBAL_UNIT_ASSIGNED_CONTEXT((#27070,#27072,#27073))
REPRESENTATION_CONTEXT('','3D')
);
#27070=(
LENGTH_UNIT()
NAMED_UNIT(*)
SI_UNIT(.CENTI.,.METRE.)
);
#27072=(
NAMED_UNIT(*)
PLANE_ANGLE_UNIT()
SI_UNIT($,.RADIAN.)
);
#27073=(
NAMED_UNIT(*)
SI_UNIT($,.STERADIAN.)
SOLID_ANGLE_UNIT()
);
#27127=SHAPE_DEFINITION_REPRESENTATION(#27215,#27404);
#27215=PRODUCT_DEFINITION_SHAPE('',$,#27481);
#27404=SHAPE_REPRESENTATION('',(#15681),#27046);
#27427=PRODUCT_DEFINITION_CONTEXT('part definition',#27657,'design');
#27481=PRODUCT_DEFINITION('Input M3 set screw','Input M3 set screw',#27557,
#27427);
#27557=PRODUCT_DEFINITION_FORMATION('',$,#27712);
#27657=APPLICATION_CONTEXT(
'Core Data for Automotive Mechanical Design Process');
#27658=PRODUCT_CONTEXT('part definition',#27657,'mechanical');
#27712=PRODUCT('Input M3 set screw','Input M3 set screw',
'Input M3 set screw',(#27658));
#27798=COLOUR_RGB('Black',0.12,0.14,0.17);
#27799=FILL_AREA_STYLE_COLOUR('',#27798);
#27800=FILL_AREA_STYLE('',(#27799));
#27801=SURFACE_STYLE_FILL_AREA(#27800);
#27802=SURFACE_SIDE_STYLE('',(#27801));
#27803=SURFACE_STYLE_USAGE(.BOTH.,#27802);
#27804=PRESENTATION_STYLE_ASSIGNMENT((#27803));
ENDSEC;
END-ISO-10303-21;
